ISO-10303-21;
HEADER;
/* Generated by software containing ST-Developer
 * from STEP Tools, Inc. (www.steptools.com) 
 */

FILE_DESCRIPTION(
/* description */ (''),
/* implementation_level */ '2;1');

FILE_NAME(
/* name */ 'Cap Screw - M6x25.step',
/* time_stamp */ '2026-10-29T16:43:51-07:00',
/* author */ (''),
/* organization */ (''),
/* preprocessor_version */ 'ST-DEVELOPER v20.2',
/* originating_system */ 'Autodesk Translation Framework v15.17.0.0',
/* authorisation */ '');

FILE_SCHEMA (('AUTOMOTIVE_DESIGN { 1 0 10303 214 3 1 1 }'));
ENDSEC;

DATA;
#10=MECHANICAL_DESIGN_GEOMETRIC_PRESENTATION_REPRESENTATION('',(#387),#10292);
#287=ORIENTED_CLOSED_SHELL('',*,#5034,.F.);
#292=BREP_WITH_VOIDS('Body1',#5033,(#287));
#315=CONICAL_SURFACE('',#5818,0.475,0.785398163397449);
#316=CONICAL_SURFACE('',#5822,0.485,0.785398163397448);
#317=CONICAL_SURFACE('',#5826,0.31,0.463647609000806);
#318=CONICAL_SURFACE('',#5830,0.27,0.785398163397448);
#341=SHAPE_REPRESENTATION_RELATIONSHIP('SRR','None',#10439,#364);
#364=ADVANCED_BREP_SHAPE_REPRESENTATION('',(#292),#10291);
#387=STYLED_ITEM('',(#10635),#292);
#530=FACE_BOUND('',#1398,.T.);
#699=PLANE('',#5816);
#700=PLANE('',#5824);
#701=PLANE('',#5832);
#702=PLANE('',#5833);
#703=PLANE('',#5834);
#704=PLANE('',#5835);
#705=PLANE('',#5836);
#706=PLANE('',#5837);
#707=PLANE('',#5838);
#708=PLANE('',#5839);
#709=PLANE('',#5840);
#981=FACE_OUTER_BOUND('',#1393,.T.);
#982=FACE_OUTER_BOUND('',#1394,.T.);
#983=FACE_OUTER_BOUND('',#1395,.T.);
#984=FACE_OUTER_BOUND('',#1396,.T.);
#985=FACE_OUTER_BOUND('',#1397,.T.);
#986=FACE_OUTER_BOUND('',#1399,.T.);
#987=FACE_OUTER_BOUND('',#1400,.T.);
#988=FACE_OUTER_BOUND('',#1401,.T.);
#989=FACE_OUTER_BOUND('',#1402,.T.);
#990=FACE_OUTER_BOUND('',#1403,.T.);
#991=FACE_OUTER_BOUND('',#1404,.T.);
#992=FACE_OUTER_BOUND('',#1405,.T.);
#993=FACE_OUTER_BOUND('',#1406,.T.);
#994=FACE_OUTER_BOUND('',#1407,.T.);
#995=FACE_OUTER_BOUND('',#1408,.T.);
#996=FACE_OUTER_BOUND('',#1409,.T.);
#997=FACE_OUTER_BOUND('',#1410,.T.);
#1393=EDGE_LOOP('',(#4573));
#1394=EDGE_LOOP('',(#4574,#4575,#4576,#4577));
#1395=EDGE_LOOP('',(#4578,#4579,#4580,#4581));
#1396=EDGE_LOOP('',(#4582,#4583,#4584,#4585));
#1397=EDGE_LOOP('',(#4586));
#1398=EDGE_LOOP('',(#4587));
#1399=EDGE_LOOP('',(#4588,#4589,#4590,#4591));
#1400=EDGE_LOOP('',(#4592,#4593,#4594,#4595));
#1401=EDGE_LOOP('',(#4596,#4597,#4598,#4599));
#1402=EDGE_LOOP('',(#4600));
#1403=EDGE_LOOP('',(#4601,#4602,#4603,#4604));
#1404=EDGE_LOOP('',(#4605,#4606,#4607,#4608));
#1405=EDGE_LOOP('',(#4609,#4610,#4611,#4612));
#1406=EDGE_LOOP('',(#4613,#4614,#4615,#4616));
#1407=EDGE_LOOP('',(#4617,#4618,#4619,#4620));
#1408=EDGE_LOOP('',(#4621,#4622,#4623,#4624));
#1409=EDGE_LOOP('',(#4625,#4626,#4627,#4628,#4629,#4630));
#1410=EDGE_LOOP('',(#4631,#4632,#4633,#4634,#4635,#4636));
#1779=LINE('',#10151,#2171);
#1780=LINE('',#10155,#2172);
#1781=LINE('',#10159,#2173);
#1782=LINE('',#10166,#2174);
#1783=LINE('',#10170,#2175);
#1784=LINE('',#10174,#2176);
#1785=LINE('',#10179,#2177);
#1786=LINE('',#10181,#2178);
#1787=LINE('',#10183,#2179);
#1788=LINE('',#10184,#2180);
#1789=LINE('',#10187,#2181);
#1790=LINE('',#10189,#2182);
#1791=LINE('',#10190,#2183);
#1792=LINE('',#10193,#2184);
#1793=LINE('',#10195,#2185);
#1794=LINE('',#10196,#2186);
#1795=LINE('',#10199,#2187);
#1796=LINE('',#10201,#2188);
#1797=LINE('',#10202,#2189);
#1798=LINE('',#10205,#2190);
#1799=LINE('',#10207,#2191);
#1800=LINE('',#10208,#2192);
#1801=LINE('',#10210,#2193);
#1802=LINE('',#10211,#2194);
#2171=VECTOR('',#7294,0.475);
#2172=VECTOR('',#7299,0.5);
#2173=VECTOR('',#7304,0.485);
#2174=VECTOR('',#7313,0.31);
#2175=VECTOR('',#7318,0.3);
#2176=VECTOR('',#7323,0.27);
#2177=VECTOR('',#7328,1.);
#2178=VECTOR('',#7329,1.);
#2179=VECTOR('',#7330,1.);
#2180=VECTOR('',#7331,1.);
#2181=VECTOR('',#7334,1.);
#2182=VECTOR('',#7335,1.);
#2183=VECTOR('',#7336,1.);
#2184=VECTOR('',#7339,1.);
#2185=VECTOR('',#7340,1.);
#2186=VECTOR('',#7341,1.);
#2187=VECTOR('',#7344,1.);
#2188=VECTOR('',#7345,1.);
#2189=VECTOR('',#7346,1.);
#2190=VECTOR('',#7349,1.);
#2191=VECTOR('',#7350,1.);
#2192=VECTOR('',#7351,1.);
#2193=VECTOR('',#7354,1.);
#2194=VECTOR('',#7355,1.);
#2386=CIRCLE('',#5817,0.45);
#2387=CIRCLE('',#5819,0.5);
#2388=CIRCLE('',#5821,0.5);
#2389=CIRCLE('',#5823,0.47);
#2390=CIRCLE('',#5825,0.32);
#2391=CIRCLE('',#5827,0.2942);
#2392=CIRCLE('',#5829,0.2942);
#2393=CIRCLE('',#5831,0.24);
#2775=VERTEX_POINT('',#10146);
#2776=VERTEX_POINT('',#10149);
#2777=VERTEX_POINT('',#10153);
#2778=VERTEX_POINT('',#10157);
#2779=VERTEX_POINT('',#10161);
#2780=VERTEX_POINT('',#10164);
#2781=VERTEX_POINT('',#10168);
#2782=VERTEX_POINT('',#10172);
#2783=VERTEX_POINT('',#10177);
#2784=VERTEX_POINT('',#10178);
#2785=VERTEX_POINT('',#10180);
#2786=VERTEX_POINT('',#10182);
#2787=VERTEX_POINT('',#10186);
#2788=VERTEX_POINT('',#10188);
#2789=VERTEX_POINT('',#10192);
#2790=VERTEX_POINT('',#10194);
#2791=VERTEX_POINT('',#10198);
#2792=VERTEX_POINT('',#10200);
#2793=VERTEX_POINT('',#10204);
#2794=VERTEX_POINT('',#10206);
#3377=EDGE_CURVE('',#2775,#2775,#2386,.T.);
#3378=EDGE_CURVE('',#2776,#2776,#2387,.T.);
#3379=EDGE_CURVE('',#2776,#2775,#1779,.T.);
#3380=EDGE_CURVE('',#2777,#2777,#2388,.T.);
#3381=EDGE_CURVE('',#2777,#2776,#1780,.T.);
#3382=EDGE_CURVE('',#2778,#2778,#2389,.T.);
#3383=EDGE_CURVE('',#2778,#2777,#1781,.T.);
#3384=EDGE_CURVE('',#2779,#2779,#2390,.T.);
#3385=EDGE_CURVE('',#2780,#2780,#2391,.F.);
#3386=EDGE_CURVE('',#2780,#2779,#1782,.T.);
#3387=EDGE_CURVE('',#2781,#2781,#2392,.F.);
#3388=EDGE_CURVE('',#2781,#2780,#1783,.T.);
#3389=EDGE_CURVE('',#2782,#2782,#2393,.T.);
#3390=EDGE_CURVE('',#2782,#2781,#1784,.T.);
#3391=EDGE_CURVE('',#2783,#2784,#1785,.T.);
#3392=EDGE_CURVE('',#2784,#2785,#1786,.T.);
#3393=EDGE_CURVE('',#2785,#2786,#1787,.T.);
#3394=EDGE_CURVE('',#2783,#2786,#1788,.T.);
#3395=EDGE_CURVE('',#2784,#2787,#1789,.T.);
#3396=EDGE_CURVE('',#2787,#2788,#1790,.T.);
#3397=EDGE_CURVE('',#2788,#2785,#1791,.T.);
#3398=EDGE_CURVE('',#2787,#2789,#1792,.T.);
#3399=EDGE_CURVE('',#2789,#2790,#1793,.T.);
#3400=EDGE_CURVE('',#2790,#2788,#1794,.T.);
#3401=EDGE_CURVE('',#2789,#2791,#1795,.T.);
#3402=EDGE_CURVE('',#2791,#2792,#1796,.T.);
#3403=EDGE_CURVE('',#2792,#2790,#1797,.T.);
#3404=EDGE_CURVE('',#2791,#2793,#1798,.T.);
#3405=EDGE_CURVE('',#2793,#2794,#1799,.T.);
#3406=EDGE_CURVE('',#2794,#2792,#1800,.T.);
#3407=EDGE_CURVE('',#2793,#2783,#1801,.T.);
#3408=EDGE_CURVE('',#2786,#2794,#1802,.T.);
#4573=ORIENTED_EDGE('',*,*,#3377,.F.);
#4574=ORIENTED_EDGE('',*,*,#3378,.F.);
#4575=ORIENTED_EDGE('',*,*,#3379,.T.);
#4576=ORIENTED_EDGE('',*,*,#3377,.T.);
#4577=ORIENTED_EDGE('',*,*,#3379,.F.);
#4578=ORIENTED_EDGE('',*,*,#3380,.F.);
#4579=ORIENTED_EDGE('',*,*,#3381,.T.);
#4580=ORIENTED_EDGE('',*,*,#3378,.T.);
#4581=ORIENTED_EDGE('',*,*,#3381,.F.);
#4582=ORIENTED_EDGE('',*,*,#3382,.F.);
#4583=ORIENTED_EDGE('',*,*,#3383,.T.);
#4584=ORIENTED_EDGE('',*,*,#3380,.T.);
#4585=ORIENTED_EDGE('',*,*,#3383,.F.);
#4586=ORIENTED_EDGE('',*,*,#3382,.T.);
#4587=ORIENTED_EDGE('',*,*,#3384,.F.);
#4588=ORIENTED_EDGE('',*,*,#3385,.F.);
#4589=ORIENTED_EDGE('',*,*,#3386,.T.);
#4590=ORIENTED_EDGE('',*,*,#3384,.T.);
#4591=ORIENTED_EDGE('',*,*,#3386,.F.);
#4592=ORIENTED_EDGE('',*,*,#3387,.F.);
#4593=ORIENTED_EDGE('',*,*,#3388,.T.);
#4594=ORIENTED_EDGE('',*,*,#3385,.T.);
#4595=ORIENTED_EDGE('',*,*,#3388,.F.);
#4596=ORIENTED_EDGE('',*,*,#3389,.F.);
#4597=ORIENTED_EDGE('',*,*,#3390,.T.);
#4598=ORIENTED_EDGE('',*,*,#3387,.T.);
#4599=ORIENTED_EDGE('',*,*,#3390,.F.);
#4600=ORIENTED_EDGE('',*,*,#3389,.T.);
#4601=ORIENTED_EDGE('',*,*,#3391,.T.);
#4602=ORIENTED_EDGE('',*,*,#3392,.T.);
#4603=ORIENTED_EDGE('',*,*,#3393,.T.);
#4604=ORIENTED_EDGE('',*,*,#3394,.F.);
#4605=ORIENTED_EDGE('',*,*,#3395,.T.);
#4606=ORIENTED_EDGE('',*,*,#3396,.T.);
#4607=ORIENTED_EDGE('',*,*,#3397,.T.);
#4608=ORIENTED_EDGE('',*,*,#3392,.F.);
#4609=ORIENTED_EDGE('',*,*,#3398,.T.);
#4610=ORIENTED_EDGE('',*,*,#3399,.T.);
#4611=ORIENTED_EDGE('',*,*,#3400,.T.);
#4612=ORIENTED_EDGE('',*,*,#3396,.F.);
#4613=ORIENTED_EDGE('',*,*,#3401,.T.);
#4614=ORIENTED_EDGE('',*,*,#3402,.T.);
#4615=ORIENTED_EDGE('',*,*,#3403,.T.);
#4616=ORIENTED_EDGE('',*,*,#3399,.F.);
#4617=ORIENTED_EDGE('',*,*,#3404,.T.);
#4618=ORIENTED_EDGE('',*,*,#3405,.T.);
#4619=ORIENTED_EDGE('',*,*,#3406,.T.);
#4620=ORIENTED_EDGE('',*,*,#3402,.F.);
#4621=ORIENTED_EDGE('',*,*,#3407,.T.);
#4622=ORIENTED_EDGE('',*,*,#3394,.T.);
#4623=ORIENTED_EDGE('',*,*,#3408,.T.);
#4624=ORIENTED_EDGE('',*,*,#3405,.F.);
#4625=ORIENTED_EDGE('',*,*,#3407,.F.);
#4626=ORIENTED_EDGE('',*,*,#3404,.F.);
#4627=ORIENTED_EDGE('',*,*,#3401,.F.);
#4628=ORIENTED_EDGE('',*,*,#3398,.F.);
#4629=ORIENTED_EDGE('',*,*,#3395,.F.);
#4630=ORIENTED_EDGE('',*,*,#3391,.F.);
#4631=ORIENTED_EDGE('',*,*,#3408,.F.);
#4632=ORIENTED_EDGE('',*,*,#3393,.F.);
#4633=ORIENTED_EDGE('',*,*,#3397,.F.);
#4634=ORIENTED_EDGE('',*,*,#3400,.F.);
#4635=ORIENTED_EDGE('',*,*,#3403,.F.);
#4636=ORIENTED_EDGE('',*,*,#3406,.F.);
#4717=CYLINDRICAL_SURFACE('',#5820,0.5);
#4718=CYLINDRICAL_SURFACE('',#5828,0.2942);
#4990=ADVANCED_FACE('',(#981),#699,.T.);
#4991=ADVANCED_FACE('',(#982),#315,.T.);
#4992=ADVANCED_FACE('',(#983),#4717,.T.);
#4993=ADVANCED_FACE('',(#984),#316,.T.);
#4994=ADVANCED_FACE('',(#985,#530),#700,.T.);
#4995=ADVANCED_FACE('',(#986),#317,.T.);
#4996=ADVANCED_FACE('',(#987),#4718,.T.);
#4997=ADVANCED_FACE('',(#988),#318,.T.);
#4998=ADVANCED_FACE('',(#989),#701,.T.);
#4999=ADVANCED_FACE('',(#990),#702,.F.);
#5000=ADVANCED_FACE('',(#991),#703,.F.);
#5001=ADVANCED_FACE('',(#992),#704,.F.);
#5002=ADVANCED_FACE('',(#993),#705,.F.);
#5003=ADVANCED_FACE('',(#994),#706,.F.);
#5004=ADVANCED_FACE('',(#995),#707,.F.);
#5005=ADVANCED_FACE('',(#996),#708,.F.);
#5006=ADVANCED_FACE('',(#997),#709,.F.);
#5033=CLOSED_SHELL('',(#4990,#4991,#4992,#4993,#4994,#4995,#4996,#4997,
#4998));
#5034=CLOSED_SHELL('',(#4999,#5000,#5001,#5002,#5003,#5004,#5005,#5006));
#5815=AXIS2_PLACEMENT_3D('',#10144,#7284,#7285);
#5816=AXIS2_PLACEMENT_3D('',#10145,#7286,#7287);
#5817=AXIS2_PLACEMENT_3D('',#10147,#7288,#7289);
#5818=AXIS2_PLACEMENT_3D('',#10148,#7290,#7291);
#5819=AXIS2_PLACEMENT_3D('',#10150,#7292,#7293);
#5820=AXIS2_PLACEMENT_3D('',#10152,#7295,#7296);
#5821=AXIS2_PLACEMENT_3D('',#10154,#7297,#7298);
#5822=AXIS2_PLACEMENT_3D('',#10156,#7300,#7301);
#5823=AXIS2_PLACEMENT_3D('',#10158,#7302,#7303);
#5824=AXIS2_PLACEMENT_3D('',#10160,#7305,#7306);
#5825=AXIS2_PLACEMENT_3D('',#10162,#7307,#7308);
#5826=AXIS2_PLACEMENT_3D('',#10163,#7309,#7310);
#5827=AXIS2_PLACEMENT_3D('',#10165,#7311,#7312);
#5828=AXIS2_PLACEMENT_3D('',#10167,#7314,#7315);
#5829=AXIS2_PLACEMENT_3D('',#10169,#7316,#7317);
#5830=AXIS2_PLACEMENT_3D('',#10171,#7319,#7320);
#5831=AXIS2_PLACEMENT_3D('',#10173,#7321,#7322);
#5832=AXIS2_PLACEMENT_3D('',#10175,#7324,#7325);
#5833=AXIS2_PLACEMENT_3D('',#10176,#7326,#7327);
#5834=AXIS2_PLACEMENT_3D('',#10185,#7332,#7333);
#5835=AXIS2_PLACEMENT_3D('',#10191,#7337,#7338);
#5836=AXIS2_PLACEMENT_3D('',#10197,#7342,#7343);
#5837=AXIS2_PLACEMENT_3D('',#10203,#7347,#7348);
#5838=AXIS2_PLACEMENT_3D('',#10209,#7352,#7353);
#5839=AXIS2_PLACEMENT_3D('',#10212,#7356,#7357);
#5840=AXIS2_PLACEMENT_3D('',#10213,#7358,#7359);
#7284=DIRECTION('axis',(0.,0.,1.));
#7285=DIRECTION('refdir',(1.,0.,0.));
#7286=DIRECTION('center_axis',(0.,1.,0.));
#7287=DIRECTION('ref_axis',(0.,0.,1.));
#7288=DIRECTION('center_axis',(0.,-1.,0.));
#7289=DIRECTION('ref_axis',(1.,0.,0.));
#7290=DIRECTION('center_axis',(0.,-1.,0.));
#7291=DIRECTION('ref_axis',(1.,0.,0.));
#7292=DIRECTION('center_axis',(0.,-1.,0.));
#7293=DIRECTION('ref_axis',(1.,0.,0.));
#7294=DIRECTION('',(0.707106781186548,0.707106781186547,8.65956056235494E-17));
#7295=DIRECTION('center_axis',(0.,-1.,0.));
#7296=DIRECTION('ref_axis',(1.,0.,0.));
#7297=DIRECTION('center_axis',(0.,-1.,0.));
#7298=DIRECTION('ref_axis',(1.,0.,0.));
#7299=DIRECTION('',(0.,1.,0.));
#7300=DIRECTION('center_axis',(0.,1.,0.));
#7301=DIRECTION('ref_axis',(1.,0.,0.));
#7302=DIRECTION('center_axis',(0.,-1.,0.));
#7303=DIRECTION('ref_axis',(1.,0.,0.));
#7304=DIRECTION('',(-0.707106781186547,0.707106781186548,-8.65956056235493E-17));
#7305=DIRECTION('center_axis',(0.,-1.,0.));
#7306=DIRECTION('ref_axis',(0.,0.,-1.));
#7307=DIRECTION('center_axis',(0.,-1.,0.));
#7308=DIRECTION('ref_axis',(1.,0.,0.));
#7309=DIRECTION('center_axis',(0.,1.,0.));
#7310=DIRECTION('ref_axis',(1.,0.,0.));
#7311=DIRECTION('center_axis',(0.,1.,0.));
#7312=DIRECTION('ref_axis',(1.,0.,0.));
#7313=DIRECTION('',(-0.447213595499958,0.894427190999916,-5.47678698264203E-17));
#7314=DIRECTION('center_axis',(0.,-1.,0.));
#7315=DIRECTION('ref_axis',(1.,0.,0.));
#7316=DIRECTION('center_axis',(0.,1.,0.));
#7317=DIRECTION('ref_axis',(1.,0.,0.));
#7318=DIRECTION('',(0.,1.,0.));
#7319=DIRECTION('center_axis',(0.,1.,0.));
#7320=DIRECTION('ref_axis',(1.,0.,0.));
#7321=DIRECTION('center_axis',(0.,-1.,0.));
#7322=DIRECTION('ref_axis',(1.,0.,0.));
#7323=DIRECTION('',(-0.707106781186547,0.707106781186548,-8.65956056235493E-17));
#7324=DIRECTION('center_axis',(0.,-1.,0.));
#7325=DIRECTION('ref_axis',(0.,0.,-1.));
#7326=DIRECTION('center_axis',(0.866025403784439,0.,-0.5));
#7327=DIRECTION('ref_axis',(0.5,0.,0.866025403784439));
#7328=DIRECTION('',(-0.5,0.,-0.866025403784439));
#7329=DIRECTION('',(0.,-1.,0.));
#7330=DIRECTION('',(0.5,0.,0.866025403784439));
#7331=DIRECTION('',(0.,-1.,0.));
#7332=DIRECTION('center_axis',(1.92296268638356E-16,0.,-1.));
#7333=DIRECTION('ref_axis',(1.,0.,1.92296268638356E-16));
#7334=DIRECTION('',(-1.,0.,-1.92296268638356E-16));
#7335=DIRECTION('',(0.,-1.,0.));
#7336=DIRECTION('',(1.,0.,1.92296268638356E-16));
#7337=DIRECTION('center_axis',(-0.866025403784439,0.,-0.5));
#7338=DIRECTION('ref_axis',(0.5,0.,-0.866025403784439));
#7339=DIRECTION('',(-0.5,0.,0.866025403784438));
#7340=DIRECTION('',(0.,-1.,0.));
#7341=DIRECTION('',(0.5,0.,-0.866025403784438));
#7342=DIRECTION('center_axis',(-0.866025403784439,0.,0.5));
#7343=DIRECTION('ref_axis',(-0.5,0.,-0.866025403784439));
#7344=DIRECTION('',(0.5,0.,0.866025403784439));
#7345=DIRECTION('',(0.,-1.,0.));
#7346=DIRECTION('',(-0.5,0.,-0.866025403784439));
#7347=DIRECTION('center_axis',(-1.92296268638356E-16,0.,1.));
#7348=DIRECTION('ref_axis',(-1.,0.,-1.92296268638356E-16));
#7349=DIRECTION('',(1.,0.,1.92296268638356E-16));
#7350=DIRECTION('',(0.,-1.,0.));
#7351=DIRECTION('',(-1.,0.,-1.92296268638356E-16));
#7352=DIRECTION('center_axis',(0.866025403784439,0.,0.5));
#7353=DIRECTION('ref_axis',(-0.5,0.,0.866025403784439));
#7354=DIRECTION('',(0.5,0.,-0.866025403784439));
#7355=DIRECTION('',(-0.5,0.,0.866025403784439));
#7356=DIRECTION('center_axis',(0.,1.,0.));
#7357=DIRECTION('ref_axis',(1.,0.,0.));
#7358=DIRECTION('center_axis',(0.,-1.,0.));
#7359=DIRECTION('ref_axis',(0.,0.,-1.));
#10144=CARTESIAN_POINT('',(0.,0.,0.));
#10145=CARTESIAN_POINT('Origin',(0.45,0.6,0.));
#10146=CARTESIAN_POINT('',(-0.45,0.6,-5.51091059616309E-17));
#10147=CARTESIAN_POINT('Origin',(0.,0.6,0.));
#10148=CARTESIAN_POINT('Origin',(0.,0.575,0.));
#10149=CARTESIAN_POINT('',(-0.5,0.55,-6.12323399573677E-17));
#10150=CARTESIAN_POINT('Origin',(0.,0.55,0.));
#10151=CARTESIAN_POINT('',(-0.475,0.575,-5.81707229594993E-17));
#10152=CARTESIAN_POINT('Origin',(0.,0.29,0.));
#10153=CARTESIAN_POINT('',(-0.5,0.0299999999999998,-6.12323399573677E-17));
#10154=CARTESIAN_POINT('Origin',(0.,0.0299999999999998,0.));
#10155=CARTESIAN_POINT('',(-0.5,0.29,-6.12323399573677E-17));
#10156=CARTESIAN_POINT('Origin',(0.,0.0150000000000001,0.));
#10157=CARTESIAN_POINT('',(-0.47,7.11236625150491E-17,-5.75583995599256E-17));
#10158=CARTESIAN_POINT('Origin',(0.,0.,0.));
#10159=CARTESIAN_POINT('',(-0.485,0.0150000000000001,-5.93953697586466E-17));
#10160=CARTESIAN_POINT('Origin',(0.32,0.,0.));
#10161=CARTESIAN_POINT('',(-0.32,-6.93889390390723E-18,-3.91886975727153E-17));
#10162=CARTESIAN_POINT('Origin',(0.,0.,0.));
#10163=CARTESIAN_POINT('Origin',(0.,-0.02,0.));
#10164=CARTESIAN_POINT('',(-0.2942,-0.0515999999999999,3.60291088309151E-17));
#10165=CARTESIAN_POINT('Origin',(0.,-0.0515999999999999,0.));
#10166=CARTESIAN_POINT('',(-0.31,-0.02,-3.7964050773568E-17));
#10167=CARTESIAN_POINT('Origin',(0.,-1.24,0.));
#10168=CARTESIAN_POINT('',(-0.2942,-2.4458,3.60291088309151E-17));
#10169=CARTESIAN_POINT('Origin',(0.,-2.4458,0.));
#10170=CARTESIAN_POINT('',(-0.2942,-1.24,-3.60291088309151E-17));
#10171=CARTESIAN_POINT('Origin',(0.,-2.47,0.));
#10172=CARTESIAN_POINT('',(-0.24,-2.5,-2.93915231795365E-17));
#10173=CARTESIAN_POINT('Origin',(0.,-2.5,0.));
#10174=CARTESIAN_POINT('',(-0.27,-2.47,-3.30654635769785E-17));
#10175=CARTESIAN_POINT('Origin',(0.,-2.5,0.));
#10176=CARTESIAN_POINT('Origin',(0.144337567297406,-0.6,-0.25));
#10177=CARTESIAN_POINT('',(0.288675134594813,-0.6,0.));
#10178=CARTESIAN_POINT('',(0.144337567297406,-0.6,-0.25));
#10179=CARTESIAN_POINT('',(0.288675134594813,-0.6,0.));
#10180=CARTESIAN_POINT('',(0.144337567297406,-0.96,-0.25));
#10181=CARTESIAN_POINT('',(0.144337567297406,-0.6,-0.25));
#10182=CARTESIAN_POINT('',(0.288675134594813,-0.96,0.));
#10183=CARTESIAN_POINT('',(0.288675134594813,-0.96,0.));
#10184=CARTESIAN_POINT('',(0.288675134594813,-0.6,0.));
#10185=CARTESIAN_POINT('Origin',(-0.144337567297406,-0.6,-0.25));
#10186=CARTESIAN_POINT('',(-0.144337567297406,-0.6,-0.25));
#10187=CARTESIAN_POINT('',(0.144337567297406,-0.6,-0.25));
#10188=CARTESIAN_POINT('',(-0.144337567297406,-0.96,-0.25));
#10189=CARTESIAN_POINT('',(-0.144337567297406,-0.6,-0.25));
#10190=CARTESIAN_POINT('',(0.144337567297406,-0.96,-0.25));
#10191=CARTESIAN_POINT('Origin',(-0.288675134594813,-0.6,-8.32667268468867E-17));
#10192=CARTESIAN_POINT('',(-0.288675134594813,-0.6,-3.53525079574969E-17));
#10193=CARTESIAN_POINT('',(-0.144337567297406,-0.6,-0.25));
#10194=CARTESIAN_POINT('',(-0.288675134594813,-0.96,-5.55111512312578E-17));
#10195=CARTESIAN_POINT('',(-0.288675134594813,-0.6,-3.53525079574969E-17));
#10196=CARTESIAN_POINT('',(-0.144337567297406,-0.96,-0.25));
#10197=CARTESIAN_POINT('Origin',(-0.144337567297407,-0.6,0.25));
#10198=CARTESIAN_POINT('',(-0.144337567297407,-0.6,0.25));
#10199=CARTESIAN_POINT('',(-0.288675134594813,-0.6,-3.53525079574969E-17));
#10200=CARTESIAN_POINT('',(-0.144337567297407,-0.96,0.25));
#10201=CARTESIAN_POINT('',(-0.144337567297407,-0.6,0.25));
#10202=CARTESIAN_POINT('',(-0.288675134594813,-0.96,-3.53525079574969E-17));
#10203=CARTESIAN_POINT('Origin',(0.144337567297406,-0.6,0.25));
#10204=CARTESIAN_POINT('',(0.144337567297406,-0.6,0.25));
#10205=CARTESIAN_POINT('',(-0.144337567297407,-0.6,0.25));
#10206=CARTESIAN_POINT('',(0.144337567297406,-0.96,0.25));
#10207=CARTESIAN_POINT('',(0.144337567297406,-0.6,0.25));
#10208=CARTESIAN_POINT('',(-0.144337567297407,-0.96,0.25));
#10209=CARTESIAN_POINT('Origin',(0.288675134594813,-0.6,0.));
#10210=CARTESIAN_POINT('',(0.144337567297406,-0.6,0.25));
#10211=CARTESIAN_POINT('',(0.144337567297406,-0.96,0.25));
#10212=CARTESIAN_POINT('Origin',(0.,-0.6,0.));
#10213=CARTESIAN_POINT('Origin',(0.,-0.96,0.));
#10263=UNCERTAINTY_MEASURE_WITH_UNIT(LENGTH_MEASURE(0.001),#10293,
'DISTANCE_ACCURACY_VALUE',
'Maximum model space distance between geometric entities at asserted c
onnectivities');
#10264=UNCERTAINTY_MEASURE_WITH_UNIT(LENGTH_MEASURE(0.001),#10293,
'DISTANCE_ACCURACY_VALUE',
'Maximum model space distance between geometric entities at asserted c
onnectivities');
#10291=(
GEOMETRIC_REPRESENTATION_CONTEXT(3)
GLOBAL_UNCERTAINTY_ASSIGNED_CONTEXT((#10263))
GLOBAL_UNIT_ASSIGNED_CONTEXT((#10293,#10295,#10296))
REPRESENTATION_CONTEXT('','3D')
);
#10292=(
GEOMETRIC_REPRESENTATION_CONTEXT(3)
GLOBAL_UNCERTAINTY_ASSIGNED_CONTEXT((#10264))
GLOBAL_UNIT_ASSIGNED_CONTEXT((#10293,#10295,#10296))
REPRESENTATION_CONTEXT('','3D')
);
#10293=(
LENGTH_UNIT()
NAMED_UNIT(*)
SI_UNIT(.CENTI.,.METRE.)
);
#10295=(
NAMED_UNIT(*)
PLANE_ANGLE_UNIT()
SI_UNIT($,.RADIAN.)
);
#10296=(
NAMED_UNIT(*)
SI_UNIT($,.STERADIAN.)
SOLID_ANGLE_UNIT()
);
#10323=SHAPE_DEFINITION_REPRESENTATION(#10389,#10439);
#10389=PRODUCT_DEFINITION_SHAPE('',$,#10467);
#10439=SHAPE_REPRESENTATION('',(#5815),#10291);
#10440=PRODUCT_DEFINITION_CONTEXT('part definition',#10523,'design');
#10467=PRODUCT_DEFINITION('Cap Screw - M6x25','Cap Screw - M6x25',
#10494,#10440);
#10494=PRODUCT_DEFINITION_FORMATION('',$,#10551);
#10523=APPLICATION_CONTEXT(
'Core Data for Automotive Mechanical Design Process');
#10524=PRODUCT_CONTEXT('part definition',#10523,'mechanical');
#10551=PRODUCT('Cap Screw - M6x25','Cap Screw - M6x25',
'Cap Screw - M6x25',(#10524));
#10629=COLOUR_RGB('Black',0.12,0.14,0.17);
#10630=FILL_AREA_STYLE_COLOUR('',#10629);
#10631=FILL_AREA_STYLE('',(#10630));
#10632=SURFACE_STYLE_FILL_AREA(#10631);
#10633=SURFACE_SIDE_STYLE('',(#10632));
#10634=SURFACE_STYLE_USAGE(.BOTH.,#10633);
#10635=PRESENTATION_STYLE_ASSIGNMENT((#10634));
ENDSEC;
END-ISO-10303-21;
